ISO-10303-21;
HEADER;
/* Generated by software containing ST-Developer
 * from STEP Tools, Inc. (www.steptools.com) 
 */

FILE_DESCRIPTION(
/* description */ ('Chute with adjustable gate'),
/* implementation_level */ '2;1');

FILE_NAME(
/* name */ 'Cap Screw - M4x16.step',
/* time_stamp */ '2026-10-27T10:52:28-07:00',
/* author */ (''),
/* organization */ (''),
/* preprocessor_version */ 'ST-DEVELOPER v20.2',
/* originating_system */ 'Autodesk Translation Framework v15.17.0.0',
/* authorisation */ '');

FILE_SCHEMA (('AUTOMOTIVE_DESIGN { 1 0 10303 214 3 1 1 }'));
ENDSEC;

DATA;
#10=MECHANICAL_DESIGN_GEOMETRIC_PRESENTATION_REPRESENTATION('',(#445),#13094);
#330=ORIENTED_CLOSED_SHELL('',*,#7632,.F.);
#342=CONICAL_SURFACE('',#8600,0.325,0.785398163397448);
#343=CONICAL_SURFACE('',#8604,0.335,0.785398163397448);
#344=CONICAL_SURFACE('',#8608,0.21,0.463647609000806);
#345=CONICAL_SURFACE('',#8612,0.18,0.785398163397448);
#349=BREP_WITH_VOIDS('Body1',#7631,(#330));
#381=SHAPE_REPRESENTATION_RELATIONSHIP('SRR','None',#13284,#413);
#413=ADVANCED_BREP_SHAPE_REPRESENTATION('',(#349),#13093);
#445=STYLED_ITEM('',(#13502),#349);
#589=FACE_BOUND('',#1847,.T.);
#903=PLANE('',#8598);
#904=PLANE('',#8606);
#905=PLANE('',#8614);
#906=PLANE('',#8615);
#907=PLANE('',#8616);
#908=PLANE('',#8617);
#909=PLANE('',#8618);
#910=PLANE('',#8619);
#911=PLANE('',#8620);
#912=PLANE('',#8621);
#913=PLANE('',#8622);
#1312=FACE_OUTER_BOUND('',#1842,.T.);
#1313=FACE_OUTER_BOUND('',#1843,.T.);
#1314=FACE_OUTER_BOUND('',#1844,.T.);
#1315=FACE_OUTER_BOUND('',#1845,.T.);
#1316=FACE_OUTER_BOUND('',#1846,.T.);
#1317=FACE_OUTER_BOUND('',#1848,.T.);
#1318=FACE_OUTER_BOUND('',#1849,.T.);
#1319=FACE_OUTER_BOUND('',#1850,.T.);
#1320=FACE_OUTER_BOUND('',#1851,.T.);
#1321=FACE_OUTER_BOUND('',#1852,.T.);
#1322=FACE_OUTER_BOUND('',#1853,.T.);
#1323=FACE_OUTER_BOUND('',#1854,.T.);
#1324=FACE_OUTER_BOUND('',#1855,.T.);
#1325=FACE_OUTER_BOUND('',#1856,.T.);
#1326=FACE_OUTER_BOUND('',#1857,.T.);
#1327=FACE_OUTER_BOUND('',#1858,.T.);
#1328=FACE_OUTER_BOUND('',#1859,.T.);
#1842=EDGE_LOOP('',(#7042));
#1843=EDGE_LOOP('',(#7043,#7044,#7045,#7046));
#1844=EDGE_LOOP('',(#7047,#7048,#7049,#7050));
#1845=EDGE_LOOP('',(#7051,#7052,#7053,#7054));
#1846=EDGE_LOOP('',(#7055));
#1847=EDGE_LOOP('',(#7056));
#1848=EDGE_LOOP('',(#7057,#7058,#7059,#7060));
#1849=EDGE_LOOP('',(#7061,#7062,#7063,#7064));
#1850=EDGE_LOOP('',(#7065,#7066,#7067,#7068));
#1851=EDGE_LOOP('',(#7069));
#1852=EDGE_LOOP('',(#7070,#7071,#7072,#7073));
#1853=EDGE_LOOP('',(#7074,#7075,#7076,#7077));
#1854=EDGE_LOOP('',(#7078,#7079,#7080,#7081));
#1855=EDGE_LOOP('',(#7082,#7083,#7084,#7085));
#1856=EDGE_LOOP('',(#7086,#7087,#7088,#7089));
#1857=EDGE_LOOP('',(#7090,#7091,#7092,#7093));
#1858=EDGE_LOOP('',(#7094,#7095,#7096,#7097,#7098,#7099));
#1859=EDGE_LOOP('',(#7100,#7101,#7102,#7103,#7104,#7105));
#2613=LINE('',#12883,#3390);
#2614=LINE('',#12887,#3391);
#2615=LINE('',#12891,#3392);
#2616=LINE('',#12898,#3393);
#2617=LINE('',#12902,#3394);
#2618=LINE('',#12906,#3395);
#2619=LINE('',#12911,#3396);
#2620=LINE('',#12913,#3397);
#2621=LINE('',#12915,#3398);
#2622=LINE('',#12916,#3399);
#2623=LINE('',#12919,#3400);
#2624=LINE('',#12921,#3401);
#2625=LINE('',#12922,#3402);
#2626=LINE('',#12925,#3403);
#2627=LINE('',#12927,#3404);
#2628=LINE('',#12928,#3405);
#2629=LINE('',#12931,#3406);
#2630=LINE('',#12933,#3407);
#2631=LINE('',#12934,#3408);
#2632=LINE('',#12937,#3409);
#2633=LINE('',#12939,#3410);
#2634=LINE('',#12940,#3411);
#2635=LINE('',#12942,#3412);
#2636=LINE('',#12943,#3413);
#3390=VECTOR('',#10683,0.325);
#3391=VECTOR('',#10688,0.35);
#3392=VECTOR('',#10693,0.335);
#3393=VECTOR('',#10702,0.21);
#3394=VECTOR('',#10707,0.2);
#3395=VECTOR('',#10712,0.18);
#3396=VECTOR('',#10717,1.);
#3397=VECTOR('',#10718,1.);
#3398=VECTOR('',#10719,1.);
#3399=VECTOR('',#10720,1.);
#3400=VECTOR('',#10723,1.);
#3401=VECTOR('',#10724,1.);
#3402=VECTOR('',#10725,1.);
#3403=VECTOR('',#10728,1.);
#3404=VECTOR('',#10729,1.);
#3405=VECTOR('',#10730,1.);
#3406=VECTOR('',#10733,1.);
#3407=VECTOR('',#10734,1.);
#3408=VECTOR('',#10735,1.);
#3409=VECTOR('',#10738,1.);
#3410=VECTOR('',#10739,1.);
#3411=VECTOR('',#10740,1.);
#3412=VECTOR('',#10743,1.);
#3413=VECTOR('',#10744,1.);
#3585=CIRCLE('',#8599,0.3);
#3586=CIRCLE('',#8601,0.35);
#3587=CIRCLE('',#8603,0.35);
#3588=CIRCLE('',#8605,0.32);
#3589=CIRCLE('',#8607,0.22);
#3590=CIRCLE('',#8609,0.1954);
#3591=CIRCLE('',#8611,0.1954);
#3592=CIRCLE('',#8613,0.16);
#4206=VERTEX_POINT('',#12878);
#4207=VERTEX_POINT('',#12881);
#4208=VERTEX_POINT('',#12885);
#4209=VERTEX_POINT('',#12889);
#4210=VERTEX_POINT('',#12893);
#4211=VERTEX_POINT('',#12896);
#4212=VERTEX_POINT('',#12900);
#4213=VERTEX_POINT('',#12904);
#4214=VERTEX_POINT('',#12909);
#4215=VERTEX_POINT('',#12910);
#4216=VERTEX_POINT('',#12912);
#4217=VERTEX_POINT('',#12914);
#4218=VERTEX_POINT('',#12918);
#4219=VERTEX_POINT('',#12920);
#4220=VERTEX_POINT('',#12924);
#4221=VERTEX_POINT('',#12926);
#4222=VERTEX_POINT('',#12930);
#4223=VERTEX_POINT('',#12932);
#4224=VERTEX_POINT('',#12936);
#4225=VERTEX_POINT('',#12938);
#5154=EDGE_CURVE('',#4206,#4206,#3585,.T.);
#5155=EDGE_CURVE('',#4207,#4207,#3586,.T.);
#5156=EDGE_CURVE('',#4207,#4206,#2613,.T.);
#5157=EDGE_CURVE('',#4208,#4208,#3587,.T.);
#5158=EDGE_CURVE('',#4208,#4207,#2614,.T.);
#5159=EDGE_CURVE('',#4209,#4209,#3588,.T.);
#5160=EDGE_CURVE('',#4209,#4208,#2615,.T.);
#5161=EDGE_CURVE('',#4210,#4210,#3589,.T.);
#5162=EDGE_CURVE('',#4211,#4211,#3590,.F.);
#5163=EDGE_CURVE('',#4211,#4210,#2616,.T.);
#5164=EDGE_CURVE('',#4212,#4212,#3591,.F.);
#5165=EDGE_CURVE('',#4212,#4211,#2617,.T.);
#5166=EDGE_CURVE('',#4213,#4213,#3592,.T.);
#5167=EDGE_CURVE('',#4213,#4212,#2618,.T.);
#5168=EDGE_CURVE('',#4214,#4215,#2619,.T.);
#5169=EDGE_CURVE('',#4215,#4216,#2620,.T.);
#5170=EDGE_CURVE('',#4216,#4217,#2621,.T.);
#5171=EDGE_CURVE('',#4214,#4217,#2622,.T.);
#5172=EDGE_CURVE('',#4215,#4218,#2623,.T.);
#5173=EDGE_CURVE('',#4218,#4219,#2624,.T.);
#5174=EDGE_CURVE('',#4219,#4216,#2625,.T.);
#5175=EDGE_CURVE('',#4218,#4220,#2626,.T.);
#5176=EDGE_CURVE('',#4220,#4221,#2627,.T.);
#5177=EDGE_CURVE('',#4221,#4219,#2628,.T.);
#5178=EDGE_CURVE('',#4220,#4222,#2629,.T.);
#5179=EDGE_CURVE('',#4222,#4223,#2630,.T.);
#5180=EDGE_CURVE('',#4223,#4221,#2631,.T.);
#5181=EDGE_CURVE('',#4222,#4224,#2632,.T.);
#5182=EDGE_CURVE('',#4224,#4225,#2633,.T.);
#5183=EDGE_CURVE('',#4225,#4223,#2634,.T.);
#5184=EDGE_CURVE('',#4224,#4214,#2635,.T.);
#5185=EDGE_CURVE('',#4217,#4225,#2636,.T.);
#7042=ORIENTED_EDGE('',*,*,#5154,.F.);
#7043=ORIENTED_EDGE('',*,*,#5155,.F.);
#7044=ORIENTED_EDGE('',*,*,#5156,.T.);
#7045=ORIENTED_EDGE('',*,*,#5154,.T.);
#7046=ORIENTED_EDGE('',*,*,#5156,.F.);
#7047=ORIENTED_EDGE('',*,*,#5157,.F.);
#7048=ORIENTED_EDGE('',*,*,#5158,.T.);
#7049=ORIENTED_EDGE('',*,*,#5155,.T.);
#7050=ORIENTED_EDGE('',*,*,#5158,.F.);
#7051=ORIENTED_EDGE('',*,*,#5159,.F.);
#7052=ORIENTED_EDGE('',*,*,#5160,.T.);
#7053=ORIENTED_EDGE('',*,*,#5157,.T.);
#7054=ORIENTED_EDGE('',*,*,#5160,.F.);
#7055=ORIENTED_EDGE('',*,*,#5159,.T.);
#7056=ORIENTED_EDGE('',*,*,#5161,.F.);
#7057=ORIENTED_EDGE('',*,*,#5162,.F.);
#7058=ORIENTED_EDGE('',*,*,#5163,.T.);
#7059=ORIENTED_EDGE('',*,*,#5161,.T.);
#7060=ORIENTED_EDGE('',*,*,#5163,.F.);
#7061=ORIENTED_EDGE('',*,*,#5164,.F.);
#7062=ORIENTED_EDGE('',*,*,#5165,.T.);
#7063=ORIENTED_EDGE('',*,*,#5162,.T.);
#7064=ORIENTED_EDGE('',*,*,#5165,.F.);
#7065=ORIENTED_EDGE('',*,*,#5166,.F.);
#7066=ORIENTED_EDGE('',*,*,#5167,.T.);
#7067=ORIENTED_EDGE('',*,*,#5164,.T.);
#7068=ORIENTED_EDGE('',*,*,#5167,.F.);
#7069=ORIENTED_EDGE('',*,*,#5166,.T.);
#7070=ORIENTED_EDGE('',*,*,#5168,.T.);
#7071=ORIENTED_EDGE('',*,*,#5169,.T.);
#7072=ORIENTED_EDGE('',*,*,#5170,.T.);
#7073=ORIENTED_EDGE('',*,*,#5171,.F.);
#7074=ORIENTED_EDGE('',*,*,#5172,.T.);
#7075=ORIENTED_EDGE('',*,*,#5173,.T.);
#7076=ORIENTED_EDGE('',*,*,#5174,.T.);
#7077=ORIENTED_EDGE('',*,*,#5169,.F.);
#7078=ORIENTED_EDGE('',*,*,#5175,.T.);
#7079=ORIENTED_EDGE('',*,*,#5176,.T.);
#7080=ORIENTED_EDGE('',*,*,#5177,.T.);
#7081=ORIENTED_EDGE('',*,*,#5173,.F.);
#7082=ORIENTED_EDGE('',*,*,#5178,.T.);
#7083=ORIENTED_EDGE('',*,*,#5179,.T.);
#7084=ORIENTED_EDGE('',*,*,#5180,.T.);
#7085=ORIENTED_EDGE('',*,*,#5176,.F.);
#7086=ORIENTED_EDGE('',*,*,#5181,.T.);
#7087=ORIENTED_EDGE('',*,*,#5182,.T.);
#7088=ORIENTED_EDGE('',*,*,#5183,.T.);
#7089=ORIENTED_EDGE('',*,*,#5179,.F.);
#7090=ORIENTED_EDGE('',*,*,#5184,.T.);
#7091=ORIENTED_EDGE('',*,*,#5171,.T.);
#7092=ORIENTED_EDGE('',*,*,#5185,.T.);
#7093=ORIENTED_EDGE('',*,*,#5182,.F.);
#7094=ORIENTED_EDGE('',*,*,#5184,.F.);
#7095=ORIENTED_EDGE('',*,*,#5181,.F.);
#7096=ORIENTED_EDGE('',*,*,#5178,.F.);
#7097=ORIENTED_EDGE('',*,*,#5175,.F.);
#7098=ORIENTED_EDGE('',*,*,#5172,.F.);
#7099=ORIENTED_EDGE('',*,*,#5168,.F.);
#7100=ORIENTED_EDGE('',*,*,#5185,.F.);
#7101=ORIENTED_EDGE('',*,*,#5170,.F.);
#7102=ORIENTED_EDGE('',*,*,#5174,.F.);
#7103=ORIENTED_EDGE('',*,*,#5177,.F.);
#7104=ORIENTED_EDGE('',*,*,#5180,.F.);
#7105=ORIENTED_EDGE('',*,*,#5183,.F.);
#7180=CYLINDRICAL_SURFACE('',#8602,0.35);
#7181=CYLINDRICAL_SURFACE('',#8610,0.1954);
#7580=ADVANCED_FACE('',(#1312),#903,.T.);
#7581=ADVANCED_FACE('',(#1313),#342,.T.);
#7582=ADVANCED_FACE('',(#1314),#7180,.T.);
#7583=ADVANCED_FACE('',(#1315),#343,.T.);
#7584=ADVANCED_FACE('',(#1316,#589),#904,.T.);
#7585=ADVANCED_FACE('',(#1317),#344,.T.);
#7586=ADVANCED_FACE('',(#1318),#7181,.T.);
#7587=ADVANCED_FACE('',(#1319),#345,.T.);
#7588=ADVANCED_FACE('',(#1320),#905,.T.);
#7589=ADVANCED_FACE('',(#1321),#906,.F.);
#7590=ADVANCED_FACE('',(#1322),#907,.F.);
#7591=ADVANCED_FACE('',(#1323),#908,.F.);
#7592=ADVANCED_FACE('',(#1324),#909,.F.);
#7593=ADVANCED_FACE('',(#1325),#910,.F.);
#7594=ADVANCED_FACE('',(#1326),#911,.F.);
#7595=ADVANCED_FACE('',(#1327),#912,.F.);
#7596=ADVANCED_FACE('',(#1328),#913,.F.);
#7631=CLOSED_SHELL('',(#7580,#7581,#7582,#7583,#7584,#7585,#7586,#7587,
#7588));
#7632=CLOSED_SHELL('',(#7589,#7590,#7591,#7592,#7593,#7594,#7595,#7596));
#8597=AXIS2_PLACEMENT_3D('',#12876,#10673,#10674);
#8598=AXIS2_PLACEMENT_3D('',#12877,#10675,#10676);
#8599=AXIS2_PLACEMENT_3D('',#12879,#10677,#10678);
#8600=AXIS2_PLACEMENT_3D('',#12880,#10679,#10680);
#8601=AXIS2_PLACEMENT_3D('',#12882,#10681,#10682);
#8602=AXIS2_PLACEMENT_3D('',#12884,#10684,#10685);
#8603=AXIS2_PLACEMENT_3D('',#12886,#10686,#10687);
#8604=AXIS2_PLACEMENT_3D('',#12888,#10689,#10690);
#8605=AXIS2_PLACEMENT_3D('',#12890,#10691,#10692);
#8606=AXIS2_PLACEMENT_3D('',#12892,#10694,#10695);
#8607=AXIS2_PLACEMENT_3D('',#12894,#10696,#10697);
#8608=AXIS2_PLACEMENT_3D('',#12895,#10698,#10699);
#8609=AXIS2_PLACEMENT_3D('',#12897,#10700,#10701);
#8610=AXIS2_PLACEMENT_3D('',#12899,#10703,#10704);
#8611=AXIS2_PLACEMENT_3D('',#12901,#10705,#10706);
#8612=AXIS2_PLACEMENT_3D('',#12903,#10708,#10709);
#8613=AXIS2_PLACEMENT_3D('',#12905,#10710,#10711);
#8614=AXIS2_PLACEMENT_3D('',#12907,#10713,#10714);
#8615=AXIS2_PLACEMENT_3D('',#12908,#10715,#10716);
#8616=AXIS2_PLACEMENT_3D('',#12917,#10721,#10722);
#8617=AXIS2_PLACEMENT_3D('',#12923,#10726,#10727);
#8618=AXIS2_PLACEMENT_3D('',#12929,#10731,#10732);
#8619=AXIS2_PLACEMENT_3D('',#12935,#10736,#10737);
#8620=AXIS2_PLACEMENT_3D('',#12941,#10741,#10742);
#8621=AXIS2_PLACEMENT_3D('',#12944,#10745,#10746);
#8622=AXIS2_PLACEMENT_3D('',#12945,#10747,#10748);
#10673=DIRECTION('axis',(0.,0.,1.));
#10674=DIRECTION('refdir',(1.,0.,0.));
#10675=DIRECTION('center_axis',(0.,1.,0.));
#10676=DIRECTION('ref_axis',(0.,0.,1.));
#10677=DIRECTION('center_axis',(0.,-1.,0.));
#10678=DIRECTION('ref_axis',(1.,0.,0.));
#10679=DIRECTION('center_axis',(0.,-1.,0.));
#10680=DIRECTION('ref_axis',(1.,0.,0.));
#10681=DIRECTION('center_axis',(0.,-1.,0.));
#10682=DIRECTION('ref_axis',(1.,0.,0.));
#10683=DIRECTION('',(0.707106781186547,0.707106781186548,8.65956056235493E-17));
#10684=DIRECTION('center_axis',(0.,-1.,0.));
#10685=DIRECTION('ref_axis',(1.,0.,0.));
#10686=DIRECTION('center_axis',(0.,-1.,0.));
#10687=DIRECTION('ref_axis',(1.,0.,0.));
#10688=DIRECTION('',(0.,1.,0.));
#10689=DIRECTION('center_axis',(0.,1.,0.));
#10690=DIRECTION('ref_axis',(1.,0.,0.));
#10691=DIRECTION('center_axis',(0.,-1.,0.));
#10692=DIRECTION('ref_axis',(1.,0.,0.));
#10693=DIRECTION('',(-0.707106781186547,0.707106781186548,-8.65956056235493E-17));
#10694=DIRECTION('center_axis',(0.,-1.,0.));
#10695=DIRECTION('ref_axis',(0.,0.,-1.));
#10696=DIRECTION('center_axis',(0.,-1.,0.));
#10697=DIRECTION('ref_axis',(1.,0.,0.));
#10698=DIRECTION('center_axis',(0.,1.,0.));
#10699=DIRECTION('ref_axis',(1.,0.,0.));
#10700=DIRECTION('center_axis',(0.,1.,0.));
#10701=DIRECTION('ref_axis',(1.,0.,0.));
#10702=DIRECTION('',(-0.447213595499958,0.894427190999916,-5.47678698264203E-17));
#10703=DIRECTION('center_axis',(0.,-1.,0.));
#10704=DIRECTION('ref_axis',(1.,0.,0.));
#10705=DIRECTION('center_axis',(0.,1.,0.));
#10706=DIRECTION('ref_axis',(1.,0.,0.));
#10707=DIRECTION('',(0.,1.,0.));
#10708=DIRECTION('center_axis',(0.,1.,0.));
#10709=DIRECTION('ref_axis',(1.,0.,0.));
#10710=DIRECTION('center_axis',(0.,-1.,0.));
#10711=DIRECTION('ref_axis',(1.,0.,0.));
#10712=DIRECTION('',(-0.707106781186547,0.707106781186548,-8.65956056235493E-17));
#10713=DIRECTION('center_axis',(0.,-1.,0.));
#10714=DIRECTION('ref_axis',(0.,0.,-1.));
#10715=DIRECTION('center_axis',(0.866025403784439,0.,-0.5));
#10716=DIRECTION('ref_axis',(0.5,0.,0.866025403784439));
#10717=DIRECTION('',(-0.5,0.,-0.866025403784439));
#10718=DIRECTION('',(0.,-1.,0.));
#10719=DIRECTION('',(0.5,0.,0.866025403784439));
#10720=DIRECTION('',(0.,-1.,0.));
#10721=DIRECTION('center_axis',(1.60246890531964E-16,0.,-1.));
#10722=DIRECTION('ref_axis',(1.,0.,1.60246890531964E-16));
#10723=DIRECTION('',(-1.,0.,-1.60246890531964E-16));
#10724=DIRECTION('',(0.,-1.,0.));
#10725=DIRECTION('',(1.,0.,1.60246890531964E-16));
#10726=DIRECTION('center_axis',(-0.866025403784439,0.,-0.5));
#10727=DIRECTION('ref_axis',(0.5,0.,-0.866025403784439));
#10728=DIRECTION('',(-0.5,0.,0.866025403784439));
#10729=DIRECTION('',(0.,-1.,0.));
#10730=DIRECTION('',(0.5,0.,-0.866025403784439));
#10731=DIRECTION('center_axis',(-0.866025403784439,0.,0.5));
#10732=DIRECTION('ref_axis',(-0.5,0.,-0.866025403784439));
#10733=DIRECTION('',(0.5,0.,0.866025403784439));
#10734=DIRECTION('',(0.,-1.,0.));
#10735=DIRECTION('',(-0.5,0.,-0.866025403784439));
#10736=DIRECTION('center_axis',(-1.60246890531964E-16,0.,1.));
#10737=DIRECTION('ref_axis',(-1.,0.,-1.60246890531964E-16));
#10738=DIRECTION('',(1.,0.,1.60246890531964E-16));
#10739=DIRECTION('',(0.,-1.,0.));
#10740=DIRECTION('',(-1.,0.,-1.60246890531964E-16));
#10741=DIRECTION('center_axis',(0.866025403784439,0.,0.5));
#10742=DIRECTION('ref_axis',(-0.5,0.,0.866025403784439));
#10743=DIRECTION('',(0.5,0.,-0.866025403784439));
#10744=DIRECTION('',(-0.5,0.,0.866025403784439));
#10745=DIRECTION('center_axis',(0.,1.,0.));
#10746=DIRECTION('ref_axis',(1.,0.,0.));
#10747=DIRECTION('center_axis',(0.,-1.,0.));
#10748=DIRECTION('ref_axis',(0.,0.,-1.));
#12876=CARTESIAN_POINT('',(0.,0.,0.));
#12877=CARTESIAN_POINT('Origin',(0.3,0.4,0.));
#12878=CARTESIAN_POINT('',(-0.3,0.4,-3.67394039744206E-17));
#12879=CARTESIAN_POINT('Origin',(0.,0.4,0.));
#12880=CARTESIAN_POINT('Origin',(0.,0.375,0.));
#12881=CARTESIAN_POINT('',(-0.35,0.35,-4.28626379701573E-17));
#12882=CARTESIAN_POINT('Origin',(0.,0.35,0.));
#12883=CARTESIAN_POINT('',(-0.325,0.375,-3.9801020972289E-17));
#12884=CARTESIAN_POINT('Origin',(0.,0.19,0.));
#12885=CARTESIAN_POINT('',(-0.35,0.03,-4.28626379701574E-17));
#12886=CARTESIAN_POINT('Origin',(0.,0.03,0.));
#12887=CARTESIAN_POINT('',(-0.35,0.19,-4.28626379701574E-17));
#12888=CARTESIAN_POINT('Origin',(0.,0.0149999999999999,0.));
#12889=CARTESIAN_POINT('',(-0.32,-3.29597460435593E-17,-3.91886975727153E-17));
#12890=CARTESIAN_POINT('Origin',(0.,0.,0.));
#12891=CARTESIAN_POINT('',(-0.335,0.0149999999999999,-4.10256677714363E-17));
#12892=CARTESIAN_POINT('Origin',(0.22,0.,0.));
#12893=CARTESIAN_POINT('',(-0.22,-6.93889390390723E-18,-2.69422295812418E-17));
#12894=CARTESIAN_POINT('Origin',(0.,0.,0.));
#12895=CARTESIAN_POINT('Origin',(0.,-0.02,0.));
#12896=CARTESIAN_POINT('',(-0.1954,-0.0492,2.39295984553393E-17));
#12897=CARTESIAN_POINT('Origin',(0.,-0.0492,0.));
#12898=CARTESIAN_POINT('',(-0.21,-0.02,-2.57175827820944E-17));
#12899=CARTESIAN_POINT('Origin',(0.,-0.8,0.));
#12900=CARTESIAN_POINT('',(-0.1954,-1.5646,2.39295984553393E-17));
#12901=CARTESIAN_POINT('Origin',(0.,-1.5646,0.));
#12902=CARTESIAN_POINT('',(-0.1954,-0.8,-2.39295984553393E-17));
#12903=CARTESIAN_POINT('Origin',(0.,-1.58,0.));
#12904=CARTESIAN_POINT('',(-0.16,-1.6,-1.95943487863577E-17));
#12905=CARTESIAN_POINT('Origin',(0.,-1.6,0.));
#12906=CARTESIAN_POINT('',(-0.18,-1.58,-2.20436423846524E-17));
#12907=CARTESIAN_POINT('Origin',(0.,-1.6,0.));
#12908=CARTESIAN_POINT('Origin',(0.0866025403784439,-0.4,-0.15));
#12909=CARTESIAN_POINT('',(0.173205080756888,-0.4,0.));
#12910=CARTESIAN_POINT('',(0.0866025403784439,-0.4,-0.15));
#12911=CARTESIAN_POINT('',(0.173205080756888,-0.4,0.));
#12912=CARTESIAN_POINT('',(0.0866025403784439,-0.64,-0.15));
#12913=CARTESIAN_POINT('',(0.0866025403784439,-0.4,-0.15));
#12914=CARTESIAN_POINT('',(0.173205080756888,-0.64,0.));
#12915=CARTESIAN_POINT('',(0.173205080756888,-0.64,0.));
#12916=CARTESIAN_POINT('',(0.173205080756888,-0.4,0.));
#12917=CARTESIAN_POINT('Origin',(-0.0866025403784438,-0.4,-0.15));
#12918=CARTESIAN_POINT('',(-0.0866025403784438,-0.4,-0.15));
#12919=CARTESIAN_POINT('',(0.0866025403784439,-0.4,-0.15));
#12920=CARTESIAN_POINT('',(-0.0866025403784438,-0.64,-0.15));
#12921=CARTESIAN_POINT('',(-0.0866025403784438,-0.4,-0.15));
#12922=CARTESIAN_POINT('',(0.0866025403784439,-0.64,-0.15));
#12923=CARTESIAN_POINT('Origin',(-0.173205080756888,-0.4,-2.77555756156289E-17));
#12924=CARTESIAN_POINT('',(-0.173205080756888,-0.4,-2.12115047744981E-17));
#12925=CARTESIAN_POINT('',(-0.0866025403784438,-0.4,-0.15));
#12926=CARTESIAN_POINT('',(-0.173205080756888,-0.64,-2.77555756156289E-17));
#12927=CARTESIAN_POINT('',(-0.173205080756888,-0.4,-2.12115047744981E-17));
#12928=CARTESIAN_POINT('',(-0.0866025403784438,-0.64,-0.15));
#12929=CARTESIAN_POINT('Origin',(-0.0866025403784439,-0.4,0.15));
#12930=CARTESIAN_POINT('',(-0.0866025403784439,-0.4,0.15));
#12931=CARTESIAN_POINT('',(-0.173205080756888,-0.4,-2.12115047744981E-17));
#12932=CARTESIAN_POINT('',(-0.0866025403784439,-0.64,0.15));
#12933=CARTESIAN_POINT('',(-0.0866025403784439,-0.4,0.15));
#12934=CARTESIAN_POINT('',(-0.173205080756888,-0.64,-2.12115047744981E-17));
#12935=CARTESIAN_POINT('Origin',(0.0866025403784439,-0.4,0.15));
#12936=CARTESIAN_POINT('',(0.0866025403784439,-0.4,0.15));
#12937=CARTESIAN_POINT('',(-0.0866025403784439,-0.4,0.15));
#12938=CARTESIAN_POINT('',(0.0866025403784439,-0.64,0.15));
#12939=CARTESIAN_POINT('',(0.0866025403784439,-0.4,0.15));
#12940=CARTESIAN_POINT('',(-0.0866025403784439,-0.64,0.15));
#12941=CARTESIAN_POINT('Origin',(0.173205080756888,-0.4,0.));
#12942=CARTESIAN_POINT('',(0.0866025403784439,-0.4,0.15));
#12943=CARTESIAN_POINT('',(0.0866025403784439,-0.64,0.15));
#12944=CARTESIAN_POINT('Origin',(0.,-0.4,-2.77555756156289E-17));
#12945=CARTESIAN_POINT('Origin',(0.,-0.64,-2.77555756156289E-17));
#13056=UNCERTAINTY_MEASURE_WITH_UNIT(LENGTH_MEASURE(0.001),#13095,
'DISTANCE_ACCURACY_VALUE',
'Maximum model space distance between geometric entities at asserted c
onnectivities');
#13057=UNCERTAINTY_MEASURE_WITH_UNIT(LENGTH_MEASURE(0.001),#13095,
'DISTANCE_ACCURACY_VALUE',
'Maximum model space distance between geometric entities at asserted c
onnectivities');
#13093=(
GEOMETRIC_REPRESENTATION_CONTEXT(3)
GLOBAL_UNCERTAINTY_ASSIGNED_CONTEXT((#13056))
GLOBAL_UNIT_ASSIGNED_CONTEXT((#13095,#13097,#13098))
REPRESENTATION_CONTEXT('','3D')
);
#13094=(
GEOMETRIC_REPRESENTATION_CONTEXT(3)
GLOBAL_UNCERTAINTY_ASSIGNED_CONTEXT((#13057))
GLOBAL_UNIT_ASSIGNED_CONTEXT((#13095,#13097,#13098))
REPRESENTATION_CONTEXT('','3D')
);
#13095=(
LENGTH_UNIT()
NAMED_UNIT(*)
SI_UNIT(.CENTI.,.METRE.)
);
#13097=(
NAMED_UNIT(*)
PLANE_ANGLE_UNIT()
SI_UNIT($,.RADIAN.)
);
#13098=(
NAMED_UNIT(*)
SI_UNIT($,.STERADIAN.)
SOLID_ANGLE_UNIT()
);
#13134=SHAPE_DEFINITION_REPRESENTATION(#13173,#13284);
#13173=PRODUCT_DEFINITION_SHAPE('',$,#13321);
#13284=SHAPE_REPRESENTATION('',(#8597),#13093);
#13285=PRODUCT_DEFINITION_CONTEXT('part definition',#13395,'design');
#13321=PRODUCT_DEFINITION('Cap Screw - M4x16','Cap Screw - M4x16',#13357,
#13285);
#13357=PRODUCT_DEFINITION_FORMATION('',$,#13432);
#13395=APPLICATION_CONTEXT(
'Core Data for Automotive Mechanical Design Process');
#13396=PRODUCT_CONTEXT('part definition',#13395,'mechanical');
#13432=PRODUCT('Cap Screw - M4x16','Cap Screw - M4x16',
'Cap Screw - M4x16',(#13396));
#13496=COLOUR_RGB('Black',0.12,0.14,0.17);
#13497=FILL_AREA_STYLE_COLOUR('',#13496);
#13498=FILL_AREA_STYLE('',(#13497));
#13499=SURFACE_STYLE_FILL_AREA(#13498);
#13500=SURFACE_SIDE_STYLE('',(#13499));
#13501=SURFACE_STYLE_USAGE(.BOTH.,#13500);
#13502=PRESENTATION_STYLE_ASSIGNMENT((#13501));
ENDSEC;
END-ISO-10303-21;
